ISO-10303-21;
HEADER;
/* Generated by software containing ST-Developer
 * from STEP Tools, Inc. (www.steptools.com) 
 */

FILE_DESCRIPTION(
/* description */ ('Y-strainer with drain'),
/* implementation_level */ '2;1');

FILE_NAME(
/* name */ 'Cap Screw - M6x25.step',
/* time_stamp */ '2026-10-28T00:41:55-07:00',
/* author */ (''),
/* organization */ (''),
/* preprocessor_version */ 'ST-DEVELOPER v20.2',
/* originating_system */ 'Autodesk Translation Framework v15.17.0.0',
/* authorisation */ '');

FILE_SCHEMA (('AUTOMOTIVE_DESIGN { 1 0 10303 214 3 1 1 }'));
ENDSEC;

DATA;
#10=MECHANICAL_DESIGN_GEOMETRIC_PRESENTATION_REPRESENTATION('',(#99),#8864);
#67=ORIENTED_CLOSED_SHELL('',*,#3390,.F.);
#68=CONICAL_SURFACE('',#3697,0.475,0.785398163397449);
#69=CONICAL_SURFACE('',#3701,0.485,0.785398163397448);
#70=CONICAL_SURFACE('',#3705,0.31,0.463647609000806);
#71=CONICAL_SURFACE('',#3709,0.27,0.785398163397448);
#74=BREP_WITH_VOIDS('Body1',#3389,(#67));
#81=SHAPE_REPRESENTATION_RELATIONSHIP('SRR','None',#8913,#90);
#90=ADVANCED_BREP_SHAPE_REPRESENTATION('',(#74),#8861);
#99=STYLED_ITEM('',(#9040),#74);
#450=FACE_BOUND('',#918,.T.);
#490=PLANE('',#3695);
#491=PLANE('',#3703);
#492=PLANE('',#3711);
#493=PLANE('',#3712);
#494=PLANE('',#3713);
#495=PLANE('',#3714);
#496=PLANE('',#3715);
#497=PLANE('',#3716);
#498=PLANE('',#3717);
#499=PLANE('',#3718);
#500=PLANE('',#3719);
#630=FACE_OUTER_BOUND('',#913,.T.);
#631=FACE_OUTER_BOUND('',#914,.T.);
#632=FACE_OUTER_BOUND('',#915,.T.);
#633=FACE_OUTER_BOUND('',#916,.T.);
#634=FACE_OUTER_BOUND('',#917,.T.);
#635=FACE_OUTER_BOUND('',#919,.T.);
#636=FACE_OUTER_BOUND('',#920,.T.);
#637=FACE_OUTER_BOUND('',#921,.T.);
#638=FACE_OUTER_BOUND('',#922,.T.);
#639=FACE_OUTER_BOUND('',#923,.T.);
#640=FACE_OUTER_BOUND('',#924,.T.);
#641=FACE_OUTER_BOUND('',#925,.T.);
#642=FACE_OUTER_BOUND('',#926,.T.);
#643=FACE_OUTER_BOUND('',#927,.T.);
#644=FACE_OUTER_BOUND('',#928,.T.);
#645=FACE_OUTER_BOUND('',#929,.T.);
#646=FACE_OUTER_BOUND('',#930,.T.);
#913=EDGE_LOOP('',(#2972));
#914=EDGE_LOOP('',(#2973,#2974,#2975,#2976));
#915=EDGE_LOOP('',(#2977,#2978,#2979,#2980));
#916=EDGE_LOOP('',(#2981,#2982,#2983,#2984));
#917=EDGE_LOOP('',(#2985));
#918=EDGE_LOOP('',(#2986));
#919=EDGE_LOOP('',(#2987,#2988,#2989,#2990));
#920=EDGE_LOOP('',(#2991,#2992,#2993,#2994));
#921=EDGE_LOOP('',(#2995,#2996,#2997,#2998));
#922=EDGE_LOOP('',(#2999));
#923=EDGE_LOOP('',(#3000,#3001,#3002,#3003));
#924=EDGE_LOOP('',(#3004,#3005,#3006,#3007));
#925=EDGE_LOOP('',(#3008,#3009,#3010,#3011));
#926=EDGE_LOOP('',(#3012,#3013,#3014,#3015));
#927=EDGE_LOOP('',(#3016,#3017,#3018,#3019));
#928=EDGE_LOOP('',(#3020,#3021,#3022,#3023));
#929=EDGE_LOOP('',(#3024,#3025,#3026,#3027,#3028,#3029));
#930=EDGE_LOOP('',(#3030,#3031,#3032,#3033,#3034,#3035));
#1058=LINE('',#8651,#1221);
#1059=LINE('',#8655,#1222);
#1060=LINE('',#8659,#1223);
#1061=LINE('',#8666,#1224);
#1062=LINE('',#8670,#1225);
#1063=LINE('',#8674,#1226);
#1064=LINE('',#8679,#1227);
#1065=LINE('',#8681,#1228);
#1066=LINE('',#8683,#1229);
#1067=LINE('',#8684,#1230);
#1068=LINE('',#8687,#1231);
#1069=LINE('',#8689,#1232);
#1070=LINE('',#8690,#1233);
#1071=LINE('',#8693,#1234);
#1072=LINE('',#8695,#1235);
#1073=LINE('',#8696,#1236);
#1074=LINE('',#8699,#1237);
#1075=LINE('',#8701,#1238);
#1076=LINE('',#8702,#1239);
#1077=LINE('',#8705,#1240);
#1078=LINE('',#8707,#1241);
#1079=LINE('',#8708,#1242);
#1080=LINE('',#8710,#1243);
#1081=LINE('',#8711,#1244);
#1221=VECTOR('',#4280,0.475);
#1222=VECTOR('',#4285,0.5);
#1223=VECTOR('',#4290,0.485);
#1224=VECTOR('',#4299,0.31);
#1225=VECTOR('',#4304,0.3);
#1226=VECTOR('',#4309,0.27);
#1227=VECTOR('',#4314,1.);
#1228=VECTOR('',#4315,1.);
#1229=VECTOR('',#4316,1.);
#1230=VECTOR('',#4317,1.);
#1231=VECTOR('',#4320,1.);
#1232=VECTOR('',#4321,1.);
#1233=VECTOR('',#4322,1.);
#1234=VECTOR('',#4325,1.);
#1235=VECTOR('',#4326,1.);
#1236=VECTOR('',#4327,1.);
#1237=VECTOR('',#4330,1.);
#1238=VECTOR('',#4331,1.);
#1239=VECTOR('',#4332,1.);
#1240=VECTOR('',#4335,1.);
#1241=VECTOR('',#4336,1.);
#1242=VECTOR('',#4337,1.);
#1243=VECTOR('',#4340,1.);
#1244=VECTOR('',#4341,1.);
#1361=CIRCLE('',#3696,0.45);
#1362=CIRCLE('',#3698,0.5);
#1363=CIRCLE('',#3700,0.5);
#1364=CIRCLE('',#3702,0.47);
#1365=CIRCLE('',#3704,0.32);
#1366=CIRCLE('',#3706,0.2942);
#1367=CIRCLE('',#3708,0.2942);
#1368=CIRCLE('',#3710,0.24);
#1667=VERTEX_POINT('',#8646);
#1668=VERTEX_POINT('',#8649);
#1669=VERTEX_POINT('',#8653);
#1670=VERTEX_POINT('',#8657);
#1671=VERTEX_POINT('',#8661);
#1672=VERTEX_POINT('',#8664);
#1673=VERTEX_POINT('',#8668);
#1674=VERTEX_POINT('',#8672);
#1675=VERTEX_POINT('',#8677);
#1676=VERTEX_POINT('',#8678);
#1677=VERTEX_POINT('',#8680);
#1678=VERTEX_POINT('',#8682);
#1679=VERTEX_POINT('',#8686);
#1680=VERTEX_POINT('',#8688);
#1681=VERTEX_POINT('',#8692);
#1682=VERTEX_POINT('',#8694);
#1683=VERTEX_POINT('',#8698);
#1684=VERTEX_POINT('',#8700);
#1685=VERTEX_POINT('',#8704);
#1686=VERTEX_POINT('',#8706);
#2110=EDGE_CURVE('',#1667,#1667,#1361,.T.);
#2111=EDGE_CURVE('',#1668,#1668,#1362,.T.);
#2112=EDGE_CURVE('',#1668,#1667,#1058,.T.);
#2113=EDGE_CURVE('',#1669,#1669,#1363,.T.);
#2114=EDGE_CURVE('',#1669,#1668,#1059,.T.);
#2115=EDGE_CURVE('',#1670,#1670,#1364,.T.);
#2116=EDGE_CURVE('',#1670,#1669,#1060,.T.);
#2117=EDGE_CURVE('',#1671,#1671,#1365,.T.);
#2118=EDGE_CURVE('',#1672,#1672,#1366,.F.);
#2119=EDGE_CURVE('',#1672,#1671,#1061,.T.);
#2120=EDGE_CURVE('',#1673,#1673,#1367,.F.);
#2121=EDGE_CURVE('',#1673,#1672,#1062,.T.);
#2122=EDGE_CURVE('',#1674,#1674,#1368,.T.);
#2123=EDGE_CURVE('',#1674,#1673,#1063,.T.);
#2124=EDGE_CURVE('',#1675,#1676,#1064,.T.);
#2125=EDGE_CURVE('',#1676,#1677,#1065,.T.);
#2126=EDGE_CURVE('',#1677,#1678,#1066,.T.);
#2127=EDGE_CURVE('',#1675,#1678,#1067,.T.);
#2128=EDGE_CURVE('',#1676,#1679,#1068,.T.);
#2129=EDGE_CURVE('',#1679,#1680,#1069,.T.);
#2130=EDGE_CURVE('',#1680,#1677,#1070,.T.);
#2131=EDGE_CURVE('',#1679,#1681,#1071,.T.);
#2132=EDGE_CURVE('',#1681,#1682,#1072,.T.);
#2133=EDGE_CURVE('',#1682,#1680,#1073,.T.);
#2134=EDGE_CURVE('',#1681,#1683,#1074,.T.);
#2135=EDGE_CURVE('',#1683,#1684,#1075,.T.);
#2136=EDGE_CURVE('',#1684,#1682,#1076,.T.);
#2137=EDGE_CURVE('',#1683,#1685,#1077,.T.);
#2138=EDGE_CURVE('',#1685,#1686,#1078,.T.);
#2139=EDGE_CURVE('',#1686,#1684,#1079,.T.);
#2140=EDGE_CURVE('',#1685,#1675,#1080,.T.);
#2141=EDGE_CURVE('',#1678,#1686,#1081,.T.);
#2972=ORIENTED_EDGE('',*,*,#2110,.F.);
#2973=ORIENTED_EDGE('',*,*,#2111,.F.);
#2974=ORIENTED_EDGE('',*,*,#2112,.T.);
#2975=ORIENTED_EDGE('',*,*,#2110,.T.);
#2976=ORIENTED_EDGE('',*,*,#2112,.F.);
#2977=ORIENTED_EDGE('',*,*,#2113,.F.);
#2978=ORIENTED_EDGE('',*,*,#2114,.T.);
#2979=ORIENTED_EDGE('',*,*,#2111,.T.);
#2980=ORIENTED_EDGE('',*,*,#2114,.F.);
#2981=ORIENTED_EDGE('',*,*,#2115,.F.);
#2982=ORIENTED_EDGE('',*,*,#2116,.T.);
#2983=ORIENTED_EDGE('',*,*,#2113,.T.);
#2984=ORIENTED_EDGE('',*,*,#2116,.F.);
#2985=ORIENTED_EDGE('',*,*,#2115,.T.);
#2986=ORIENTED_EDGE('',*,*,#2117,.F.);
#2987=ORIENTED_EDGE('',*,*,#2118,.F.);
#2988=ORIENTED_EDGE('',*,*,#2119,.T.);
#2989=ORIENTED_EDGE('',*,*,#2117,.T.);
#2990=ORIENTED_EDGE('',*,*,#2119,.F.);
#2991=ORIENTED_EDGE('',*,*,#2120,.F.);
#2992=ORIENTED_EDGE('',*,*,#2121,.T.);
#2993=ORIENTED_EDGE('',*,*,#2118,.T.);
#2994=ORIENTED_EDGE('',*,*,#2121,.F.);
#2995=ORIENTED_EDGE('',*,*,#2122,.F.);
#2996=ORIENTED_EDGE('',*,*,#2123,.T.);
#2997=ORIENTED_EDGE('',*,*,#2120,.T.);
#2998=ORIENTED_EDGE('',*,*,#2123,.F.);
#2999=ORIENTED_EDGE('',*,*,#2122,.T.);
#3000=ORIENTED_EDGE('',*,*,#2124,.T.);
#3001=ORIENTED_EDGE('',*,*,#2125,.T.);
#3002=ORIENTED_EDGE('',*,*,#2126,.T.);
#3003=ORIENTED_EDGE('',*,*,#2127,.F.);
#3004=ORIENTED_EDGE('',*,*,#2128,.T.);
#3005=ORIENTED_EDGE('',*,*,#2129,.T.);
#3006=ORIENTED_EDGE('',*,*,#2130,.T.);
#3007=ORIENTED_EDGE('',*,*,#2125,.F.);
#3008=ORIENTED_EDGE('',*,*,#2131,.T.);
#3009=ORIENTED_EDGE('',*,*,#2132,.T.);
#3010=ORIENTED_EDGE('',*,*,#2133,.T.);
#3011=ORIENTED_EDGE('',*,*,#2129,.F.);
#3012=ORIENTED_EDGE('',*,*,#2134,.T.);
#3013=ORIENTED_EDGE('',*,*,#2135,.T.);
#3014=ORIENTED_EDGE('',*,*,#2136,.T.);
#3015=ORIENTED_EDGE('',*,*,#2132,.F.);
#3016=ORIENTED_EDGE('',*,*,#2137,.T.);
#3017=ORIENTED_EDGE('',*,*,#2138,.T.);
#3018=ORIENTED_EDGE('',*,*,#2139,.T.);
#3019=ORIENTED_EDGE('',*,*,#2135,.F.);
#3020=ORIENTED_EDGE('',*,*,#2140,.T.);
#3021=ORIENTED_EDGE('',*,*,#2127,.T.);
#3022=ORIENTED_EDGE('',*,*,#2141,.T.);
#3023=ORIENTED_EDGE('',*,*,#2138,.F.);
#3024=ORIENTED_EDGE('',*,*,#2140,.F.);
#3025=ORIENTED_EDGE('',*,*,#2137,.F.);
#3026=ORIENTED_EDGE('',*,*,#2134,.F.);
#3027=ORIENTED_EDGE('',*,*,#2131,.F.);
#3028=ORIENTED_EDGE('',*,*,#2128,.F.);
#3029=ORIENTED_EDGE('',*,*,#2124,.F.);
#3030=ORIENTED_EDGE('',*,*,#2141,.F.);
#3031=ORIENTED_EDGE('',*,*,#2126,.F.);
#3032=ORIENTED_EDGE('',*,*,#2130,.F.);
#3033=ORIENTED_EDGE('',*,*,#2133,.F.);
#3034=ORIENTED_EDGE('',*,*,#2136,.F.);
#3035=ORIENTED_EDGE('',*,*,#2139,.F.);
#3225=CYLINDRICAL_SURFACE('',#3699,0.5);
#3226=CYLINDRICAL_SURFACE('',#3707,0.2942);
#3341=ADVANCED_FACE('',(#630),#490,.T.);
#3342=ADVANCED_FACE('',(#631),#68,.T.);
#3343=ADVANCED_FACE('',(#632),#3225,.T.);
#3344=ADVANCED_FACE('',(#633),#69,.T.);
#3345=ADVANCED_FACE('',(#634,#450),#491,.T.);
#3346=ADVANCED_FACE('',(#635),#70,.T.);
#3347=ADVANCED_FACE('',(#636),#3226,.T.);
#3348=ADVANCED_FACE('',(#637),#71,.T.);
#3349=ADVANCED_FACE('',(#638),#492,.T.);
#3350=ADVANCED_FACE('',(#639),#493,.F.);
#3351=ADVANCED_FACE('',(#640),#494,.F.);
#3352=ADVANCED_FACE('',(#641),#495,.F.);
#3353=ADVANCED_FACE('',(#642),#496,.F.);
#3354=ADVANCED_FACE('',(#643),#497,.F.);
#3355=ADVANCED_FACE('',(#644),#498,.F.);
#3356=ADVANCED_FACE('',(#645),#499,.F.);
#3357=ADVANCED_FACE('',(#646),#500,.F.);
#3389=CLOSED_SHELL('',(#3341,#3342,#3343,#3344,#3345,#3346,#3347,#3348,
#3349));
#3390=CLOSED_SHELL('',(#3350,#3351,#3352,#3353,#3354,#3355,#3356,#3357));
#3694=AXIS2_PLACEMENT_3D('',#8644,#4270,#4271);
#3695=AXIS2_PLACEMENT_3D('',#8645,#4272,#4273);
#3696=AXIS2_PLACEMENT_3D('',#8647,#4274,#4275);
#3697=AXIS2_PLACEMENT_3D('',#8648,#4276,#4277);
#3698=AXIS2_PLACEMENT_3D('',#8650,#4278,#4279);
#3699=AXIS2_PLACEMENT_3D('',#8652,#4281,#4282);
#3700=AXIS2_PLACEMENT_3D('',#8654,#4283,#4284);
#3701=AXIS2_PLACEMENT_3D('',#8656,#4286,#4287);
#3702=AXIS2_PLACEMENT_3D('',#8658,#4288,#4289);
#3703=AXIS2_PLACEMENT_3D('',#8660,#4291,#4292);
#3704=AXIS2_PLACEMENT_3D('',#8662,#4293,#4294);
#3705=AXIS2_PLACEMENT_3D('',#8663,#4295,#4296);
#3706=AXIS2_PLACEMENT_3D('',#8665,#4297,#4298);
#3707=AXIS2_PLACEMENT_3D('',#8667,#4300,#4301);
#3708=AXIS2_PLACEMENT_3D('',#8669,#4302,#4303);
#3709=AXIS2_PLACEMENT_3D('',#8671,#4305,#4306);
#3710=AXIS2_PLACEMENT_3D('',#8673,#4307,#4308);
#3711=AXIS2_PLACEMENT_3D('',#8675,#4310,#4311);
#3712=AXIS2_PLACEMENT_3D('',#8676,#4312,#4313);
#3713=AXIS2_PLACEMENT_3D('',#8685,#4318,#4319);
#3714=AXIS2_PLACEMENT_3D('',#8691,#4323,#4324);
#3715=AXIS2_PLACEMENT_3D('',#8697,#4328,#4329);
#3716=AXIS2_PLACEMENT_3D('',#8703,#4333,#4334);
#3717=AXIS2_PLACEMENT_3D('',#8709,#4338,#4339);
#3718=AXIS2_PLACEMENT_3D('',#8712,#4342,#4343);
#3719=AXIS2_PLACEMENT_3D('',#8713,#4344,#4345);
#4270=DIRECTION('axis',(0.,0.,1.));
#4271=DIRECTION('refdir',(1.,0.,0.));
#4272=DIRECTION('center_axis',(0.,1.,0.));
#4273=DIRECTION('ref_axis',(0.,0.,1.));
#4274=DIRECTION('center_axis',(0.,-1.,0.));
#4275=DIRECTION('ref_axis',(1.,0.,0.));
#4276=DIRECTION('center_axis',(0.,-1.,0.));
#4277=DIRECTION('ref_axis',(1.,0.,0.));
#4278=DIRECTION('center_axis',(0.,-1.,0.));
#4279=DIRECTION('ref_axis',(1.,0.,0.));
#4280=DIRECTION('',(0.707106781186548,0.707106781186547,8.65956056235494E-17));
#4281=DIRECTION('center_axis',(0.,-1.,0.));
#4282=DIRECTION('ref_axis',(1.,0.,0.));
#4283=DIRECTION('center_axis',(0.,-1.,0.));
#4284=DIRECTION('ref_axis',(1.,0.,0.));
#4285=DIRECTION('',(0.,1.,0.));
#4286=DIRECTION('center_axis',(0.,1.,0.));
#4287=DIRECTION('ref_axis',(1.,0.,0.));
#4288=DIRECTION('center_axis',(0.,-1.,0.));
#4289=DIRECTION('ref_axis',(1.,0.,0.));
#4290=DIRECTION('',(-0.707106781186547,0.707106781186548,-8.65956056235493E-17));
#4291=DIRECTION('center_axis',(0.,-1.,0.));
#4292=DIRECTION('ref_axis',(0.,0.,-1.));
#4293=DIRECTION('center_axis',(0.,-1.,0.));
#4294=DIRECTION('ref_axis',(1.,0.,0.));
#4295=DIRECTION('center_axis',(0.,1.,0.));
#4296=DIRECTION('ref_axis',(1.,0.,0.));
#4297=DIRECTION('center_axis',(0.,1.,0.));
#4298=DIRECTION('ref_axis',(1.,0.,0.));
#4299=DIRECTION('',(-0.447213595499958,0.894427190999916,-5.47678698264203E-17));
#4300=DIRECTION('center_axis',(0.,-1.,0.));
#4301=DIRECTION('ref_axis',(1.,0.,0.));
#4302=DIRECTION('center_axis',(0.,1.,0.));
#4303=DIRECTION('ref_axis',(1.,0.,0.));
#4304=DIRECTION('',(0.,1.,0.));
#4305=DIRECTION('center_axis',(0.,1.,0.));
#4306=DIRECTION('ref_axis',(1.,0.,0.));
#4307=DIRECTION('center_axis',(0.,-1.,0.));
#4308=DIRECTION('ref_axis',(1.,0.,0.));
#4309=DIRECTION('',(-0.707106781186547,0.707106781186548,-8.65956056235493E-17));
#4310=DIRECTION('center_axis',(0.,-1.,0.));
#4311=DIRECTION('ref_axis',(0.,0.,-1.));
#4312=DIRECTION('center_axis',(0.866025403784439,0.,-0.5));
#4313=DIRECTION('ref_axis',(0.5,0.,0.866025403784439));
#4314=DIRECTION('',(-0.5,0.,-0.866025403784439));
#4315=DIRECTION('',(0.,-1.,0.));
#4316=DIRECTION('',(0.5,0.,0.866025403784439));
#4317=DIRECTION('',(0.,-1.,0.));
#4318=DIRECTION('center_axis',(1.92296268638356E-16,0.,-1.));
#4319=DIRECTION('ref_axis',(1.,0.,1.92296268638356E-16));
#4320=DIRECTION('',(-1.,0.,-1.92296268638356E-16));
#4321=DIRECTION('',(0.,-1.,0.));
#4322=DIRECTION('',(1.,0.,1.92296268638356E-16));
#4323=DIRECTION('center_axis',(-0.866025403784439,0.,-0.5));
#4324=DIRECTION('ref_axis',(0.5,0.,-0.866025403784439));
#4325=DIRECTION('',(-0.5,0.,0.866025403784438));
#4326=DIRECTION('',(0.,-1.,0.));
#4327=DIRECTION('',(0.5,0.,-0.866025403784438));
#4328=DIRECTION('center_axis',(-0.866025403784439,0.,0.5));
#4329=DIRECTION('ref_axis',(-0.5,0.,-0.866025403784439));
#4330=DIRECTION('',(0.5,0.,0.866025403784439));
#4331=DIRECTION('',(0.,-1.,0.));
#4332=DIRECTION('',(-0.5,0.,-0.866025403784439));
#4333=DIRECTION('center_axis',(-1.92296268638356E-16,0.,1.));
#4334=DIRECTION('ref_axis',(-1.,0.,-1.92296268638356E-16));
#4335=DIRECTION('',(1.,0.,1.92296268638356E-16));
#4336=DIRECTION('',(0.,-1.,0.));
#4337=DIRECTION('',(-1.,0.,-1.92296268638356E-16));
#4338=DIRECTION('center_axis',(0.866025403784439,0.,0.5));
#4339=DIRECTION('ref_axis',(-0.5,0.,0.866025403784439));
#4340=DIRECTION('',(0.5,0.,-0.866025403784439));
#4341=DIRECTION('',(-0.5,0.,0.866025403784439));
#4342=DIRECTION('center_axis',(0.,1.,0.));
#4343=DIRECTION('ref_axis',(1.,0.,0.));
#4344=DIRECTION('center_axis',(0.,-1.,0.));
#4345=DIRECTION('ref_axis',(0.,0.,-1.));
#8644=CARTESIAN_POINT('',(0.,0.,0.));
#8645=CARTESIAN_POINT('Origin',(0.45,0.6,0.));
#8646=CARTESIAN_POINT('',(-0.45,0.6,-5.51091059616309E-17));
#8647=CARTESIAN_POINT('Origin',(0.,0.6,0.));
#8648=CARTESIAN_POINT('Origin',(0.,0.575,0.));
#8649=CARTESIAN_POINT('',(-0.5,0.55,-6.12323399573677E-17));
#8650=CARTESIAN_POINT('Origin',(0.,0.55,0.));
#8651=CARTESIAN_POINT('',(-0.475,0.575,-5.81707229594993E-17));
#8652=CARTESIAN_POINT('Origin',(0.,0.29,0.));
#8653=CARTESIAN_POINT('',(-0.5,0.0299999999999998,-6.12323399573677E-17));
#8654=CARTESIAN_POINT('Origin',(0.,0.0299999999999998,0.));
#8655=CARTESIAN_POINT('',(-0.5,0.29,-6.12323399573677E-17));
#8656=CARTESIAN_POINT('Origin',(0.,0.0150000000000001,0.));
#8657=CARTESIAN_POINT('',(-0.47,7.11236625150491E-17,-5.75583995599256E-17));
#8658=CARTESIAN_POINT('Origin',(0.,0.,0.));
#8659=CARTESIAN_POINT('',(-0.485,0.0150000000000001,-5.93953697586466E-17));
#8660=CARTESIAN_POINT('Origin',(0.32,0.,0.));
#8661=CARTESIAN_POINT('',(-0.32,-6.93889390390723E-18,-3.91886975727153E-17));
#8662=CARTESIAN_POINT('Origin',(0.,0.,0.));
#8663=CARTESIAN_POINT('Origin',(0.,-0.02,0.));
#8664=CARTESIAN_POINT('',(-0.2942,-0.0515999999999999,3.60291088309151E-17));
#8665=CARTESIAN_POINT('Origin',(0.,-0.0515999999999999,0.));
#8666=CARTESIAN_POINT('',(-0.31,-0.02,-3.7964050773568E-17));
#8667=CARTESIAN_POINT('Origin',(0.,-1.24,0.));
#8668=CARTESIAN_POINT('',(-0.2942,-2.4458,3.60291088309151E-17));
#8669=CARTESIAN_POINT('Origin',(0.,-2.4458,0.));
#8670=CARTESIAN_POINT('',(-0.2942,-1.24,-3.60291088309151E-17));
#8671=CARTESIAN_POINT('Origin',(0.,-2.47,0.));
#8672=CARTESIAN_POINT('',(-0.24,-2.5,-2.93915231795365E-17));
#8673=CARTESIAN_POINT('Origin',(0.,-2.5,0.));
#8674=CARTESIAN_POINT('',(-0.27,-2.47,-3.30654635769785E-17));
#8675=CARTESIAN_POINT('Origin',(0.,-2.5,0.));
#8676=CARTESIAN_POINT('Origin',(0.144337567297406,-0.6,-0.25));
#8677=CARTESIAN_POINT('',(0.288675134594813,-0.6,0.));
#8678=CARTESIAN_POINT('',(0.144337567297406,-0.6,-0.25));
#8679=CARTESIAN_POINT('',(0.288675134594813,-0.6,0.));
#8680=CARTESIAN_POINT('',(0.144337567297406,-0.96,-0.25));
#8681=CARTESIAN_POINT('',(0.144337567297406,-0.6,-0.25));
#8682=CARTESIAN_POINT('',(0.288675134594813,-0.96,0.));
#8683=CARTESIAN_POINT('',(0.288675134594813,-0.96,0.));
#8684=CARTESIAN_POINT('',(0.288675134594813,-0.6,0.));
#8685=CARTESIAN_POINT('Origin',(-0.144337567297406,-0.6,-0.25));
#8686=CARTESIAN_POINT('',(-0.144337567297406,-0.6,-0.25));
#8687=CARTESIAN_POINT('',(0.144337567297406,-0.6,-0.25));
#8688=CARTESIAN_POINT('',(-0.144337567297406,-0.96,-0.25));
#8689=CARTESIAN_POINT('',(-0.144337567297406,-0.6,-0.25));
#8690=CARTESIAN_POINT('',(0.144337567297406,-0.96,-0.25));
#8691=CARTESIAN_POINT('Origin',(-0.288675134594813,-0.6,-8.32667268468867E-17));
#8692=CARTESIAN_POINT('',(-0.288675134594813,-0.6,-3.53525079574969E-17));
#8693=CARTESIAN_POINT('',(-0.144337567297406,-0.6,-0.25));
#8694=CARTESIAN_POINT('',(-0.288675134594813,-0.96,-5.55111512312578E-17));
#8695=CARTESIAN_POINT('',(-0.288675134594813,-0.6,-3.53525079574969E-17));
#8696=CARTESIAN_POINT('',(-0.144337567297406,-0.96,-0.25));
#8697=CARTESIAN_POINT('Origin',(-0.144337567297407,-0.6,0.25));
#8698=CARTESIAN_POINT('',(-0.144337567297407,-0.6,0.25));
#8699=CARTESIAN_POINT('',(-0.288675134594813,-0.6,-3.53525079574969E-17));
#8700=CARTESIAN_POINT('',(-0.144337567297407,-0.96,0.25));
#8701=CARTESIAN_POINT('',(-0.144337567297407,-0.6,0.25));
#8702=CARTESIAN_POINT('',(-0.288675134594813,-0.96,-3.53525079574969E-17));
#8703=CARTESIAN_POINT('Origin',(0.144337567297406,-0.6,0.25));
#8704=CARTESIAN_POINT('',(0.144337567297406,-0.6,0.25));
#8705=CARTESIAN_POINT('',(-0.144337567297407,-0.6,0.25));
#8706=CARTESIAN_POINT('',(0.144337567297406,-0.96,0.25));
#8707=CARTESIAN_POINT('',(0.144337567297406,-0.6,0.25));
#8708=CARTESIAN_POINT('',(-0.144337567297407,-0.96,0.25));
#8709=CARTESIAN_POINT('Origin',(0.288675134594813,-0.6,0.));
#8710=CARTESIAN_POINT('',(0.144337567297406,-0.6,0.25));
#8711=CARTESIAN_POINT('',(0.144337567297406,-0.96,0.25));
#8712=CARTESIAN_POINT('Origin',(0.,-0.6,0.));
#8713=CARTESIAN_POINT('Origin',(0.,-0.96,0.));
#8849=UNCERTAINTY_MEASURE_WITH_UNIT(LENGTH_MEASURE(0.001),#8865,
'DISTANCE_ACCURACY_VALUE',
'Maximum model space distance between geometric entities at asserted c
onnectivities');
#8852=UNCERTAINTY_MEASURE_WITH_UNIT(LENGTH_MEASURE(0.001),#8865,
'DISTANCE_ACCURACY_VALUE',
'Maximum model space distance between geometric entities at asserted c
onnectivities');
#8861=(
GEOMETRIC_REPRESENTATION_CONTEXT(3)
GLOBAL_UNCERTAINTY_ASSIGNED_CONTEXT((#8849))
GLOBAL_UNIT_ASSIGNED_CONTEXT((#8865,#8867,#8868))
REPRESENTATION_CONTEXT('','3D')
);
#8864=(
GEOMETRIC_REPRESENTATION_CONTEXT(3)
GLOBAL_UNCERTAINTY_ASSIGNED_CONTEXT((#8852))
GLOBAL_UNIT_ASSIGNED_CONTEXT((#8865,#8867,#8868))
REPRESENTATION_CONTEXT('','3D')
);
#8865=(
LENGTH_UNIT()
NAMED_UNIT(*)
SI_UNIT(.CENTI.,.METRE.)
);
#8867=(
NAMED_UNIT(*)
PLANE_ANGLE_UNIT()
SI_UNIT($,.RADIAN.)
);
#8868=(
NAMED_UNIT(*)
SI_UNIT($,.STERADIAN.)
SOLID_ANGLE_UNIT()
);
#8877=SHAPE_DEFINITION_REPRESENTATION(#8888,#8913);
#8888=PRODUCT_DEFINITION_SHAPE('',$,#8925);
#8913=SHAPE_REPRESENTATION('',(#3694),#8861);
#8916=PRODUCT_DEFINITION_CONTEXT('part definition',#8951,'design');
#8925=PRODUCT_DEFINITION('Cap Screw - M6x25','Cap Screw - M6x25',#8936,
#8916);
#8936=PRODUCT_DEFINITION_FORMATION('',$,#8961);
#8951=APPLICATION_CONTEXT(
'Core Data for Automotive Mechanical Design Process');
#8952=PRODUCT_CONTEXT('part definition',#8951,'mechanical');
#8961=PRODUCT('Cap Screw - M6x25','Cap Screw - M6x25',
'Cap Screw - M6x25',(#8952));
#9034=COLOUR_RGB('Black',0.12,0.14,0.17);
#9035=FILL_AREA_STYLE_COLOUR('',#9034);
#9036=FILL_AREA_STYLE('',(#9035));
#9037=SURFACE_STYLE_FILL_AREA(#9036);
#9038=SURFACE_SIDE_STYLE('',(#9037));
#9039=SURFACE_STYLE_USAGE(.BOTH.,#9038);
#9040=PRESENTATION_STYLE_ASSIGNMENT((#9039));
ENDSEC;
END-ISO-10303-21;
